ISO-10303-21;
HEADER;
/* Generated by software containing ST-Developer
 * from STEP Tools, Inc. (www.steptools.com) 
 */

FILE_DESCRIPTION(
/* description */ (''),
/* implementation_level */ '2;1');

FILE_NAME(
/* name */ 'Ring (1).step',
/* time_stamp */ '2026-10-22T15:07:41+06:00',
/* author */ (''),
/* organization */ (''),
/* preprocessor_version */ 'ST-DEVELOPER v20.2',
/* originating_system */ 'Autodesk Translation Framework v15.15.0.0',
/* authorisation */ '');

FILE_SCHEMA (('AUTOMOTIVE_DESIGN { 1 0 10303 214 3 1 1 }'));
ENDSEC;

DATA;
#10=MECHANICAL_DESIGN_GEOMETRIC_PRESENTATION_REPRESENTATION('',(#2879),#19220);
#68=SHAPE_REPRESENTATION_RELATIONSHIP('SRR','None',#19271,#82);
#82=ADVANCED_BREP_SHAPE_REPRESENTATION('',(#96),#19207);
#96=MANIFOLD_SOLID_BREP('Ring',#11315);
#110=FACE_BOUND('',#3453,.T.);
#111=FACE_BOUND('',#3456,.T.);
#112=FACE_BOUND('',#3458,.T.);
#113=FACE_BOUND('',#3460,.T.);
#114=FACE_BOUND('',#3464,.T.);
#115=FACE_BOUND('',#3467,.T.);
#116=FACE_BOUND('',#3472,.T.);
#117=FACE_BOUND('',#3475,.T.);
#629=PLANE('',#11523);
#630=PLANE('',#11528);
#631=PLANE('',#11530);
#632=PLANE('',#11533);
#633=PLANE('',#11538);
#634=PLANE('',#11543);
#635=PLANE('',#11550);
#636=PLANE('',#11554);
#843=LINE('',#16142,#1698);
#844=LINE('',#16158,#1699);
#845=LINE('',#16160,#1700);
#846=LINE('',#16169,#1701);
#847=LINE('',#16175,#1702);
#848=LINE('',#16180,#1703);
#849=LINE('',#16182,#1704);
#850=LINE('',#16189,#1705);
#1698=VECTOR('',#12820,20.7480593298244);
#1699=VECTOR('',#12841,20.7480593298244);
#1700=VECTOR('',#12844,16.7480593298244);
#1701=VECTOR('',#12855,20.7480593298244);
#1702=VECTOR('',#12862,15.7480593298244);
#1703=VECTOR('',#12869,15.7480593298244);
#1704=VECTOR('',#12872,16.7480593298244);
#1705=VECTOR('',#12881,6.);
#2553=CYLINDRICAL_SURFACE('',#11526,20.7480593298244);
#2554=CYLINDRICAL_SURFACE('',#11536,20.7480593298244);
#2555=CYLINDRICAL_SURFACE('',#11537,16.7480593298244);
#2556=CYLINDRICAL_SURFACE('',#11541,20.7480593298244);
#2557=CYLINDRICAL_SURFACE('',#11545,15.7480593298244);
#2558=CYLINDRICAL_SURFACE('',#11547,15.7480593298244);
#2559=CYLINDRICAL_SURFACE('',#11549,16.7480593298244);
#2560=CYLINDRICAL_SURFACE('',#11552,6.);
#2879=STYLED_ITEM('',(#19389),#96);
#2905=FACE_OUTER_BOUND('',#3452,.T.);
#2906=FACE_OUTER_BOUND('',#3454,.T.);
#2907=FACE_OUTER_BOUND('',#3455,.T.);
#2908=FACE_OUTER_BOUND('',#3457,.T.);
#2909=FACE_OUTER_BOUND('',#3459,.T.);
#2910=FACE_OUTER_BOUND('',#3461,.T.);
#2911=FACE_OUTER_BOUND('',#3462,.T.);
#2912=FACE_OUTER_BOUND('',#3463,.T.);
#2913=FACE_OUTER_BOUND('',#3465,.T.);
#2914=FACE_OUTER_BOUND('',#3466,.T.);
#2915=FACE_OUTER_BOUND('',#3468,.T.);
#2916=FACE_OUTER_BOUND('',#3469,.T.);
#2917=FACE_OUTER_BOUND('',#3470,.T.);
#2918=FACE_OUTER_BOUND('',#3471,.T.);
#2919=FACE_OUTER_BOUND('',#3473,.T.);
#2920=FACE_OUTER_BOUND('',#3474,.T.);
#3452=EDGE_LOOP('',(#7768));
#3453=EDGE_LOOP('',(#7769));
#3454=EDGE_LOOP('',(#7770,#7771,#7772,#7773));
#3455=EDGE_LOOP('',(#7774));
#3456=EDGE_LOOP('',(#7775));
#3457=EDGE_LOOP('',(#7776));
#3458=EDGE_LOOP('',(#7777));
#3459=EDGE_LOOP('',(#7778));
#3460=EDGE_LOOP('',(#7779));
#3461=EDGE_LOOP('',(#7780,#7781,#7782,#7783));
#3462=EDGE_LOOP('',(#7784,#7785,#7786,#7787));
#3463=EDGE_LOOP('',(#7788));
#3464=EDGE_LOOP('',(#7789));
#3465=EDGE_LOOP('',(#7790,#7791,#7792,#7793));
#3466=EDGE_LOOP('',(#7794));
#3467=EDGE_LOOP('',(#7795));
#3468=EDGE_LOOP('',(#7796,#7797,#7798,#7799));
#3469=EDGE_LOOP('',(#7800,#7801,#7802,#7803));
#3470=EDGE_LOOP('',(#7804,#7805,#7806,#7807));
#3471=EDGE_LOOP('',(#7808));
#3472=EDGE_LOOP('',(#7809));
#3473=EDGE_LOOP('',(#7810,#7811,#7812,#7813));
#3474=EDGE_LOOP('',(#7814));
#3475=EDGE_LOOP('',(#7815));
#4525=CIRCLE('',#11524,20.7480593298244);
#4526=CIRCLE('',#11525,16.7480593298244);
#4527=CIRCLE('',#11527,20.7480593298244);
#4528=CIRCLE('',#11529,15.7480593298244);
#4529=CIRCLE('',#11531,20.7480593298244);
#4530=CIRCLE('',#11532,16.7480593298244);
#4531=CIRCLE('',#11534,20.7480593298244);
#4532=CIRCLE('',#11535,16.7480593298244);
#4533=CIRCLE('',#11539,20.7480593298244);
#4534=CIRCLE('',#11540,16.7480593298244);
#4535=CIRCLE('',#11542,20.7480593298244);
#4536=CIRCLE('',#11544,15.7480593298244);
#4537=CIRCLE('',#11546,15.7480593298244);
#4538=CIRCLE('',#11548,15.7480593298244);
#4539=CIRCLE('',#11551,6.);
#4540=CIRCLE('',#11553,6.);
#5189=VERTEX_POINT('',#16136);
#5190=VERTEX_POINT('',#16138);
#5191=VERTEX_POINT('',#16141);
#5192=VERTEX_POINT('',#16145);
#5193=VERTEX_POINT('',#16148);
#5194=VERTEX_POINT('',#16150);
#5195=VERTEX_POINT('',#16153);
#5196=VERTEX_POINT('',#16155);
#5197=VERTEX_POINT('',#16162);
#5198=VERTEX_POINT('',#16164);
#5199=VERTEX_POINT('',#16167);
#5200=VERTEX_POINT('',#16171);
#5201=VERTEX_POINT('',#16174);
#5202=VERTEX_POINT('',#16178);
#5203=VERTEX_POINT('',#16184);
#5204=VERTEX_POINT('',#16187);
#6215=EDGE_CURVE('',#5189,#5189,#4525,.T.);
#6216=EDGE_CURVE('',#5190,#5190,#4526,.T.);
#6217=EDGE_CURVE('',#5189,#5191,#843,.T.);
#6218=EDGE_CURVE('',#5191,#5191,#4527,.T.);
#6219=EDGE_CURVE('',#5192,#5192,#4528,.T.);
#6220=EDGE_CURVE('',#5193,#5193,#4529,.T.);
#6221=EDGE_CURVE('',#5194,#5194,#4530,.T.);
#6222=EDGE_CURVE('',#5195,#5195,#4531,.T.);
#6223=EDGE_CURVE('',#5196,#5196,#4532,.T.);
#6224=EDGE_CURVE('',#5193,#5195,#844,.T.);
#6225=EDGE_CURVE('',#5190,#5196,#845,.T.);
#6226=EDGE_CURVE('',#5197,#5197,#4533,.T.);
#6227=EDGE_CURVE('',#5198,#5198,#4534,.T.);
#6228=EDGE_CURVE('',#5199,#5199,#4535,.T.);
#6229=EDGE_CURVE('',#5199,#5197,#846,.T.);
#6230=EDGE_CURVE('',#5200,#5200,#4536,.T.);
#6231=EDGE_CURVE('',#5192,#5201,#847,.T.);
#6232=EDGE_CURVE('',#5201,#5201,#4537,.T.);
#6233=EDGE_CURVE('',#5202,#5202,#4538,.T.);
#6234=EDGE_CURVE('',#5202,#5200,#848,.T.);
#6235=EDGE_CURVE('',#5194,#5198,#849,.T.);
#6236=EDGE_CURVE('',#5203,#5203,#4539,.T.);
#6237=EDGE_CURVE('',#5204,#5204,#4540,.T.);
#6238=EDGE_CURVE('',#5204,#5203,#850,.T.);
#7768=ORIENTED_EDGE('',*,*,#6215,.T.);
#7769=ORIENTED_EDGE('',*,*,#6216,.F.);
#7770=ORIENTED_EDGE('',*,*,#6215,.F.);
#7771=ORIENTED_EDGE('',*,*,#6217,.T.);
#7772=ORIENTED_EDGE('',*,*,#6218,.T.);
#7773=ORIENTED_EDGE('',*,*,#6217,.F.);
#7774=ORIENTED_EDGE('',*,*,#6218,.F.);
#7775=ORIENTED_EDGE('',*,*,#6219,.T.);
#7776=ORIENTED_EDGE('',*,*,#6220,.T.);
#7777=ORIENTED_EDGE('',*,*,#6221,.F.);
#7778=ORIENTED_EDGE('',*,*,#6222,.F.);
#7779=ORIENTED_EDGE('',*,*,#6223,.F.);
#7780=ORIENTED_EDGE('',*,*,#6220,.F.);
#7781=ORIENTED_EDGE('',*,*,#6224,.T.);
#7782=ORIENTED_EDGE('',*,*,#6222,.T.);
#7783=ORIENTED_EDGE('',*,*,#6224,.F.);
#7784=ORIENTED_EDGE('',*,*,#6216,.T.);
#7785=ORIENTED_EDGE('',*,*,#6225,.T.);
#7786=ORIENTED_EDGE('',*,*,#6223,.T.);
#7787=ORIENTED_EDGE('',*,*,#6225,.F.);
#7788=ORIENTED_EDGE('',*,*,#6226,.F.);
#7789=ORIENTED_EDGE('',*,*,#6227,.T.);
#7790=ORIENTED_EDGE('',*,*,#6228,.F.);
#7791=ORIENTED_EDGE('',*,*,#6229,.T.);
#7792=ORIENTED_EDGE('',*,*,#6226,.T.);
#7793=ORIENTED_EDGE('',*,*,#6229,.F.);
#7794=ORIENTED_EDGE('',*,*,#6228,.T.);
#7795=ORIENTED_EDGE('',*,*,#6230,.T.);
#7796=ORIENTED_EDGE('',*,*,#6219,.F.);
#7797=ORIENTED_EDGE('',*,*,#6231,.T.);
#7798=ORIENTED_EDGE('',*,*,#6232,.F.);
#7799=ORIENTED_EDGE('',*,*,#6231,.F.);
#7800=ORIENTED_EDGE('',*,*,#6233,.T.);
#7801=ORIENTED_EDGE('',*,*,#6234,.T.);
#7802=ORIENTED_EDGE('',*,*,#6230,.F.);
#7803=ORIENTED_EDGE('',*,*,#6234,.F.);
#7804=ORIENTED_EDGE('',*,*,#6221,.T.);
#7805=ORIENTED_EDGE('',*,*,#6235,.T.);
#7806=ORIENTED_EDGE('',*,*,#6227,.F.);
#7807=ORIENTED_EDGE('',*,*,#6235,.F.);
#7808=ORIENTED_EDGE('',*,*,#6233,.F.);
#7809=ORIENTED_EDGE('',*,*,#6236,.F.);
#7810=ORIENTED_EDGE('',*,*,#6237,.F.);
#7811=ORIENTED_EDGE('',*,*,#6238,.T.);
#7812=ORIENTED_EDGE('',*,*,#6236,.T.);
#7813=ORIENTED_EDGE('',*,*,#6238,.F.);
#7814=ORIENTED_EDGE('',*,*,#6232,.T.);
#7815=ORIENTED_EDGE('',*,*,#6237,.T.);
#10781=ADVANCED_FACE('',(#2905,#110),#629,.T.);
#10782=ADVANCED_FACE('',(#2906),#2553,.T.);
#10783=ADVANCED_FACE('',(#2907,#111),#630,.F.);
#10784=ADVANCED_FACE('',(#2908,#112),#631,.T.);
#10785=ADVANCED_FACE('',(#2909,#113),#632,.F.);
#10786=ADVANCED_FACE('',(#2910),#2554,.T.);
#10787=ADVANCED_FACE('',(#2911),#2555,.T.);
#10788=ADVANCED_FACE('',(#2912,#114),#633,.F.);
#10789=ADVANCED_FACE('',(#2913),#2556,.T.);
#10790=ADVANCED_FACE('',(#2914,#115),#634,.T.);
#10791=ADVANCED_FACE('',(#2915),#2557,.F.);
#10792=ADVANCED_FACE('',(#2916),#2558,.F.);
#10793=ADVANCED_FACE('',(#2917),#2559,.T.);
#10794=ADVANCED_FACE('',(#2918,#116),#635,.T.);
#10795=ADVANCED_FACE('',(#2919),#2560,.F.);
#10796=ADVANCED_FACE('',(#2920,#117),#636,.F.);
#11315=CLOSED_SHELL('',(#10781,#10782,#10783,#10784,#10785,#10786,#10787,
#10788,#10789,#10790,#10791,#10792,#10793,#10794,#10795,#10796));
#11522=AXIS2_PLACEMENT_3D('',#16134,#12810,#12811);
#11523=AXIS2_PLACEMENT_3D('',#16135,#12812,#12813);
#11524=AXIS2_PLACEMENT_3D('',#16137,#12814,#12815);
#11525=AXIS2_PLACEMENT_3D('',#16139,#12816,#12817);
#11526=AXIS2_PLACEMENT_3D('',#16140,#12818,#12819);
#11527=AXIS2_PLACEMENT_3D('',#16143,#12821,#12822);
#11528=AXIS2_PLACEMENT_3D('',#16144,#12823,#12824);
#11529=AXIS2_PLACEMENT_3D('',#16146,#12825,#12826);
#11530=AXIS2_PLACEMENT_3D('',#16147,#12827,#12828);
#11531=AXIS2_PLACEMENT_3D('',#16149,#12829,#12830);
#11532=AXIS2_PLACEMENT_3D('',#16151,#12831,#12832);
#11533=AXIS2_PLACEMENT_3D('',#16152,#12833,#12834);
#11534=AXIS2_PLACEMENT_3D('',#16154,#12835,#12836);
#11535=AXIS2_PLACEMENT_3D('',#16156,#12837,#12838);
#11536=AXIS2_PLACEMENT_3D('',#16157,#12839,#12840);
#11537=AXIS2_PLACEMENT_3D('',#16159,#12842,#12843);
#11538=AXIS2_PLACEMENT_3D('',#16161,#12845,#12846);
#11539=AXIS2_PLACEMENT_3D('',#16163,#12847,#12848);
#11540=AXIS2_PLACEMENT_3D('',#16165,#12849,#12850);
#11541=AXIS2_PLACEMENT_3D('',#16166,#12851,#12852);
#11542=AXIS2_PLACEMENT_3D('',#16168,#12853,#12854);
#11543=AXIS2_PLACEMENT_3D('',#16170,#12856,#12857);
#11544=AXIS2_PLACEMENT_3D('',#16172,#12858,#12859);
#11545=AXIS2_PLACEMENT_3D('',#16173,#12860,#12861);
#11546=AXIS2_PLACEMENT_3D('',#16176,#12863,#12864);
#11547=AXIS2_PLACEMENT_3D('',#16177,#12865,#12866);
#11548=AXIS2_PLACEMENT_3D('',#16179,#12867,#12868);
#11549=AXIS2_PLACEMENT_3D('',#16181,#12870,#12871);
#11550=AXIS2_PLACEMENT_3D('',#16183,#12873,#12874);
#11551=AXIS2_PLACEMENT_3D('',#16185,#12875,#12876);
#11552=AXIS2_PLACEMENT_3D('',#16186,#12877,#12878);
#11553=AXIS2_PLACEMENT_3D('',#16188,#12879,#12880);
#11554=AXIS2_PLACEMENT_3D('',#16190,#12882,#12883);
#12810=DIRECTION('axis',(0.,0.,1.));
#12811=DIRECTION('refdir',(1.,0.,0.));
#12812=DIRECTION('center_axis',(0.,1.,0.));
#12813=DIRECTION('ref_axis',(-1.,0.,0.));
#12814=DIRECTION('center_axis',(0.,1.,0.));
#12815=DIRECTION('ref_axis',(-1.,0.,0.));
#12816=DIRECTION('center_axis',(0.,1.,0.));
#12817=DIRECTION('ref_axis',(-1.,0.,0.));
#12818=DIRECTION('center_axis',(0.,1.,0.));
#12819=DIRECTION('ref_axis',(-1.,0.,0.));
#12820=DIRECTION('',(0.,-1.,0.));
#12821=DIRECTION('center_axis',(0.,1.,0.));
#12822=DIRECTION('ref_axis',(-1.,0.,0.));
#12823=DIRECTION('center_axis',(0.,1.,0.));
#12824=DIRECTION('ref_axis',(-1.,0.,0.));
#12825=DIRECTION('center_axis',(0.,1.,0.));
#12826=DIRECTION('ref_axis',(-1.,0.,0.));
#12827=DIRECTION('center_axis',(0.,1.,0.));
#12828=DIRECTION('ref_axis',(-1.,0.,0.));
#12829=DIRECTION('center_axis',(0.,1.,0.));
#12830=DIRECTION('ref_axis',(-1.,0.,0.));
#12831=DIRECTION('center_axis',(0.,1.,0.));
#12832=DIRECTION('ref_axis',(-1.,0.,0.));
#12833=DIRECTION('center_axis',(0.,1.,0.));
#12834=DIRECTION('ref_axis',(-1.,0.,0.));
#12835=DIRECTION('center_axis',(0.,1.,0.));
#12836=DIRECTION('ref_axis',(-1.,0.,0.));
#12837=DIRECTION('center_axis',(0.,-1.,0.));
#12838=DIRECTION('ref_axis',(-1.,0.,0.));
#12839=DIRECTION('center_axis',(0.,1.,0.));
#12840=DIRECTION('ref_axis',(-1.,0.,0.));
#12841=DIRECTION('',(0.,-1.,0.));
#12842=DIRECTION('center_axis',(0.,-1.,0.));
#12843=DIRECTION('ref_axis',(-1.,0.,0.));
#12844=DIRECTION('',(0.,1.,0.));
#12845=DIRECTION('center_axis',(0.,1.,0.));
#12846=DIRECTION('ref_axis',(-1.,0.,0.));
#12847=DIRECTION('center_axis',(0.,1.,0.));
#12848=DIRECTION('ref_axis',(-1.,0.,0.));
#12849=DIRECTION('center_axis',(0.,1.,0.));
#12850=DIRECTION('ref_axis',(-1.,0.,0.));
#12851=DIRECTION('center_axis',(0.,1.,0.));
#12852=DIRECTION('ref_axis',(-1.,0.,0.));
#12853=DIRECTION('center_axis',(0.,1.,0.));
#12854=DIRECTION('ref_axis',(-1.,0.,0.));
#12855=DIRECTION('',(0.,-1.,0.));
#12856=DIRECTION('center_axis',(0.,1.,0.));
#12857=DIRECTION('ref_axis',(-1.,0.,0.));
#12858=DIRECTION('center_axis',(0.,-1.,0.));
#12859=DIRECTION('ref_axis',(-1.,0.,0.));
#12860=DIRECTION('center_axis',(0.,-1.,0.));
#12861=DIRECTION('ref_axis',(-1.,0.,0.));
#12862=DIRECTION('',(0.,1.,0.));
#12863=DIRECTION('center_axis',(0.,-1.,0.));
#12864=DIRECTION('ref_axis',(-1.,0.,0.));
#12865=DIRECTION('center_axis',(0.,-1.,0.));
#12866=DIRECTION('ref_axis',(-1.,0.,0.));
#12867=DIRECTION('center_axis',(0.,-1.,0.));
#12868=DIRECTION('ref_axis',(-1.,0.,0.));
#12869=DIRECTION('',(0.,1.,0.));
#12870=DIRECTION('center_axis',(0.,-1.,0.));
#12871=DIRECTION('ref_axis',(-1.,0.,0.));
#12872=DIRECTION('',(0.,1.,0.));
#12873=DIRECTION('center_axis',(0.,1.,0.));
#12874=DIRECTION('ref_axis',(-1.,0.,0.));
#12875=DIRECTION('center_axis',(0.,1.,0.));
#12876=DIRECTION('ref_axis',(-1.,0.,0.));
#12877=DIRECTION('center_axis',(0.,-1.,0.));
#12878=DIRECTION('ref_axis',(-1.,0.,0.));
#12879=DIRECTION('center_axis',(0.,1.,0.));
#12880=DIRECTION('ref_axis',(-1.,0.,0.));
#12881=DIRECTION('',(0.,1.,0.));
#12882=DIRECTION('center_axis',(0.,1.,0.));
#12883=DIRECTION('ref_axis',(-1.,0.,0.));
#16134=CARTESIAN_POINT('',(0.,0.,0.));
#16135=CARTESIAN_POINT('Origin',(24.1201056133058,58.,35.8480593298244));
#16136=CARTESIAN_POINT('',(44.8681649431302,58.,35.8480593298243));
#16137=CARTESIAN_POINT('Origin',(24.1201056133058,58.,35.8480593298244));
#16138=CARTESIAN_POINT('',(40.8681649431302,58.,35.8480593298244));
#16139=CARTESIAN_POINT('Origin',(24.1201056133058,58.,35.8480593298244));
#16140=CARTESIAN_POINT('Origin',(24.1201056133058,57.,35.8480593298244));
#16141=CARTESIAN_POINT('',(44.8681649431302,57.,35.8480593298243));
#16142=CARTESIAN_POINT('',(44.8681649431302,57.,35.8480593298243));
#16143=CARTESIAN_POINT('Origin',(24.1201056133058,57.,35.8480593298244));
#16144=CARTESIAN_POINT('Origin',(24.1201056133058,57.,35.8480593298244));
#16145=CARTESIAN_POINT('',(39.8681649431302,57.,35.8480593298244));
#16146=CARTESIAN_POINT('Origin',(24.1201056133058,57.,35.8480593298244));
#16147=CARTESIAN_POINT('Origin',(24.1201056133058,66.,35.8480593298244));
#16148=CARTESIAN_POINT('',(44.8681649431302,66.,35.8480593298243));
#16149=CARTESIAN_POINT('Origin',(24.1201056133058,66.,35.8480593298244));
#16150=CARTESIAN_POINT('',(40.8681649431302,66.,35.8480593298244));
#16151=CARTESIAN_POINT('Origin',(24.1201056133058,66.,35.8480593298244));
#16152=CARTESIAN_POINT('Origin',(24.1201056133058,65.,35.8480593298244));
#16153=CARTESIAN_POINT('',(44.8681649431302,65.,35.8480593298243));
#16154=CARTESIAN_POINT('Origin',(24.1201056133058,65.,35.8480593298244));
#16155=CARTESIAN_POINT('',(40.8681649431302,65.,35.8480593298244));
#16156=CARTESIAN_POINT('Origin',(24.1201056133058,65.,35.8480593298244));
#16157=CARTESIAN_POINT('Origin',(24.1201056133058,65.,35.8480593298244));
#16158=CARTESIAN_POINT('',(44.8681649431302,65.,35.8480593298243));
#16159=CARTESIAN_POINT('Origin',(24.1201056133058,72.,35.8480593298244));
#16160=CARTESIAN_POINT('',(40.8681649431302,72.,35.8480593298244));
#16161=CARTESIAN_POINT('Origin',(24.1201056133058,72.,35.8480593298244));
#16162=CARTESIAN_POINT('',(44.8681649431302,72.,35.8480593298243));
#16163=CARTESIAN_POINT('Origin',(24.1201056133058,72.,35.8480593298244));
#16164=CARTESIAN_POINT('',(40.8681649431302,72.,35.8480593298244));
#16165=CARTESIAN_POINT('Origin',(24.1201056133058,72.,35.8480593298244));
#16166=CARTESIAN_POINT('Origin',(24.1201056133058,72.,35.8480593298244));
#16167=CARTESIAN_POINT('',(44.8681649431302,73.,35.8480593298243));
#16168=CARTESIAN_POINT('Origin',(24.1201056133058,73.,35.8480593298244));
#16169=CARTESIAN_POINT('',(44.8681649431302,72.,35.8480593298243));
#16170=CARTESIAN_POINT('Origin',(24.1201056133058,73.,35.8480593298244));
#16171=CARTESIAN_POINT('',(39.8681649431302,73.,35.8480593298244));
#16172=CARTESIAN_POINT('Origin',(24.1201056133058,73.,35.8480593298244));
#16173=CARTESIAN_POINT('Origin',(24.1201056133058,72.,35.8480593298244));
#16174=CARTESIAN_POINT('',(39.8681649431302,65.,35.8480593298244));
#16175=CARTESIAN_POINT('',(39.8681649431302,72.,35.8480593298244));
#16176=CARTESIAN_POINT('Origin',(24.1201056133058,65.,35.8480593298244));
#16177=CARTESIAN_POINT('Origin',(24.1201056133058,72.,35.8480593298244));
#16178=CARTESIAN_POINT('',(39.8681649431302,66.,35.8480593298244));
#16179=CARTESIAN_POINT('Origin',(24.1201056133058,66.,35.8480593298244));
#16180=CARTESIAN_POINT('',(39.8681649431302,72.,35.8480593298244));
#16181=CARTESIAN_POINT('Origin',(24.1201056133058,72.,35.8480593298244));
#16182=CARTESIAN_POINT('',(40.8681649431302,72.,35.8480593298244));
#16183=CARTESIAN_POINT('Origin',(24.1201056133058,66.,35.8480593298244));
#16184=CARTESIAN_POINT('',(30.1201056133058,66.,35.8480593298244));
#16185=CARTESIAN_POINT('Origin',(24.1201056133058,66.,35.8480593298244));
#16186=CARTESIAN_POINT('Origin',(24.1201056133058,72.,35.8480593298244));
#16187=CARTESIAN_POINT('',(30.1201056133058,65.,35.8480593298244));
#16188=CARTESIAN_POINT('Origin',(24.1201056133058,65.,35.8480593298244));
#16189=CARTESIAN_POINT('',(30.1201056133058,72.,35.8480593298244));
#16190=CARTESIAN_POINT('Origin',(24.1201056133058,65.,35.8480593298244));
#19191=UNCERTAINTY_MEASURE_WITH_UNIT(LENGTH_MEASURE(0.01),#19221,
'DISTANCE_ACCURACY_VALUE',
'Maximum model space distance between geometric entities at asserted c
onnectivities');
#19204=UNCERTAINTY_MEASURE_WITH_UNIT(LENGTH_MEASURE(0.01),#19221,
'DISTANCE_ACCURACY_VALUE',
'Maximum model space distance between geometric entities at asserted c
onnectivities');
#19207=(
GEOMETRIC_REPRESENTATION_CONTEXT(3)
GLOBAL_UNCERTAINTY_ASSIGNED_CONTEXT((#19191))
GLOBAL_UNIT_ASSIGNED_CONTEXT((#19221,#19223,#19224))
REPRESENTATION_CONTEXT('','3D')
);
#19220=(
GEOMETRIC_REPRESENTATION_CONTEXT(3)
GLOBAL_UNCERTAINTY_ASSIGNED_CONTEXT((#19204))
GLOBAL_UNIT_ASSIGNED_CONTEXT((#19221,#19223,#19224))
REPRESENTATION_CONTEXT('','3D')
);
#19221=(
LENGTH_UNIT()
NAMED_UNIT(*)
SI_UNIT(.MILLI.,.METRE.)
);
#19223=(
NAMED_UNIT(*)
PLANE_ANGLE_UNIT()
SI_UNIT($,.RADIAN.)
);
#19224=(
NAMED_UNIT(*)
SI_UNIT($,.STERADIAN.)
SOLID_ANGLE_UNIT()
);
#19227=SHAPE_DEFINITION_REPRESENTATION(#19242,#19271);
#19242=PRODUCT_DEFINITION_SHAPE('',$,#19287);
#19271=SHAPE_REPRESENTATION('',(#11522),#19207);
#19284=PRODUCT_DEFINITION_CONTEXT('part definition',#19331,'design');
#19287=PRODUCT_DEFINITION('Ring (1)','Ring (1)',#19302,#19284);
#19302=PRODUCT_DEFINITION_FORMATION('',$,#19335);
#19331=APPLICATION_CONTEXT(
'Core Data for Automotive Mechanical Design Process');
#19332=PRODUCT_CONTEXT('part definition',#19331,'mechanical');
#19335=PRODUCT('Ring (1)','Ring (1)',$,(#19332));
#19383=COLOUR_RGB('Light Blue',0.38,0.62,0.78);
#19384=FILL_AREA_STYLE_COLOUR('',#19383);
#19385=FILL_AREA_STYLE('',(#19384));
#19386=SURFACE_STYLE_FILL_AREA(#19385);
#19387=SURFACE_SIDE_STYLE('',(#19386));
#19388=SURFACE_STYLE_USAGE(.BOTH.,#19387);
#19389=PRESENTATION_STYLE_ASSIGNMENT((#19388));
ENDSEC;
END-ISO-10303-21;
